ISO-10303-21;
HEADER;
/* Generated by software containing ST-Developer
 * from STEP Tools, Inc. (www.steptools.com) 
 */

FILE_DESCRIPTION(
/* description */ (''),
/* implementation_level */ '2;1');

FILE_NAME(
/* name */ 'Pivot thrust washer.step',
/* time_stamp */ '2026-11-12T00:53:40-08:00',
/* author */ (''),
/* organization */ (''),
/* preprocessor_version */ 'ST-DEVELOPER v20.2',
/* originating_system */ 'Autodesk Translation Framework v15.17.0.0',
/* authorisation */ '');

FILE_SCHEMA (('AUTOMOTIVE_DESIGN { 1 0 10303 214 3 1 1 }'));
ENDSEC;

DATA;
#10=MECHANICAL_DESIGN_GEOMETRIC_PRESENTATION_REPRESENTATION('',(#580),#22129);
#562=SHAPE_REPRESENTATION_RELATIONSHIP('SRR','None',#22182,#571);
#571=ADVANCED_BREP_SHAPE_REPRESENTATION('',(#589),#22128);
#580=STYLED_ITEM('',(#22238),#589);
#589=MANIFOLD_SOLID_BREP('Body1',#8811);
#649=FACE_BOUND('',#1927,.T.);
#650=FACE_BOUND('',#1929,.T.);
#901=PLANE('',#9490);
#902=PLANE('',#9491);
#1382=FACE_OUTER_BOUND('',#1924,.T.);
#1383=FACE_OUTER_BOUND('',#1925,.T.);
#1384=FACE_OUTER_BOUND('',#1926,.T.);
#1385=FACE_OUTER_BOUND('',#1928,.T.);
#1924=EDGE_LOOP('',(#8174,#8175,#8176,#8177));
#1925=EDGE_LOOP('',(#8178,#8179,#8180,#8181));
#1926=EDGE_LOOP('',(#8182));
#1927=EDGE_LOOP('',(#8183));
#1928=EDGE_LOOP('',(#8184));
#1929=EDGE_LOOP('',(#8185));
#2658=LINE('',#22088,#3388);
#2659=LINE('',#22094,#3389);
#3388=VECTOR('',#11376,0.41);
#3389=VECTOR('',#11383,0.6);
#3544=CIRCLE('',#9485,0.41);
#3545=CIRCLE('',#9486,0.41);
#3546=CIRCLE('',#9488,0.6);
#3547=CIRCLE('',#9489,0.6);
#4372=VERTEX_POINT('',#22085);
#4373=VERTEX_POINT('',#22087);
#4374=VERTEX_POINT('',#22091);
#4375=VERTEX_POINT('',#22093);
#5640=EDGE_CURVE('',#4372,#4372,#3544,.T.);
#5641=EDGE_CURVE('',#4372,#4373,#2658,.T.);
#5642=EDGE_CURVE('',#4373,#4373,#3545,.T.);
#5643=EDGE_CURVE('',#4374,#4374,#3546,.T.);
#5644=EDGE_CURVE('',#4374,#4375,#2659,.T.);
#5645=EDGE_CURVE('',#4375,#4375,#3547,.T.);
#8174=ORIENTED_EDGE('',*,*,#5640,.F.);
#8175=ORIENTED_EDGE('',*,*,#5641,.T.);
#8176=ORIENTED_EDGE('',*,*,#5642,.T.);
#8177=ORIENTED_EDGE('',*,*,#5641,.F.);
#8178=ORIENTED_EDGE('',*,*,#5643,.F.);
#8179=ORIENTED_EDGE('',*,*,#5644,.T.);
#8180=ORIENTED_EDGE('',*,*,#5645,.T.);
#8181=ORIENTED_EDGE('',*,*,#5644,.F.);
#8182=ORIENTED_EDGE('',*,*,#5643,.T.);
#8183=ORIENTED_EDGE('',*,*,#5640,.T.);
#8184=ORIENTED_EDGE('',*,*,#5645,.F.);
#8185=ORIENTED_EDGE('',*,*,#5642,.F.);
#8318=CYLINDRICAL_SURFACE('',#9484,0.41);
#8319=CYLINDRICAL_SURFACE('',#9487,0.6);
#8799=ADVANCED_FACE('',(#1382),#8318,.F.);
#8800=ADVANCED_FACE('',(#1383),#8319,.T.);
#8801=ADVANCED_FACE('',(#1384,#649),#901,.T.);
#8802=ADVANCED_FACE('',(#1385,#650),#902,.F.);
#8811=CLOSED_SHELL('',(#8799,#8800,#8801,#8802));
#9483=AXIS2_PLACEMENT_3D('',#22083,#11370,#11371);
#9484=AXIS2_PLACEMENT_3D('',#22084,#11372,#11373);
#9485=AXIS2_PLACEMENT_3D('',#22086,#11374,#11375);
#9486=AXIS2_PLACEMENT_3D('',#22089,#11377,#11378);
#9487=AXIS2_PLACEMENT_3D('',#22090,#11379,#11380);
#9488=AXIS2_PLACEMENT_3D('',#22092,#11381,#11382);
#9489=AXIS2_PLACEMENT_3D('',#22095,#11384,#11385);
#9490=AXIS2_PLACEMENT_3D('',#22096,#11386,#11387);
#9491=AXIS2_PLACEMENT_3D('',#22097,#11388,#11389);
#11370=DIRECTION('axis',(0.,0.,1.));
#11371=DIRECTION('refdir',(1.,0.,0.));
#11372=DIRECTION('center_axis',(0.,0.,1.));
#11373=DIRECTION('ref_axis',(1.,0.,0.));
#11374=DIRECTION('center_axis',(0.,0.,-1.));
#11375=DIRECTION('ref_axis',(1.,0.,0.));
#11376=DIRECTION('',(0.,0.,-1.));
#11377=DIRECTION('center_axis',(0.,0.,-1.));
#11378=DIRECTION('ref_axis',(1.,0.,0.));
#11379=DIRECTION('center_axis',(0.,0.,1.));
#11380=DIRECTION('ref_axis',(1.,0.,0.));
#11381=DIRECTION('center_axis',(0.,0.,1.));
#11382=DIRECTION('ref_axis',(1.,0.,0.));
#11383=DIRECTION('',(0.,0.,-1.));
#11384=DIRECTION('center_axis',(0.,0.,1.));
#11385=DIRECTION('ref_axis',(1.,0.,0.));
#11386=DIRECTION('center_axis',(0.,0.,1.));
#11387=DIRECTION('ref_axis',(1.,0.,0.));
#11388=DIRECTION('center_axis',(0.,0.,1.));
#11389=DIRECTION('ref_axis',(1.,0.,0.));
#22083=CARTESIAN_POINT('',(0.,0.,0.));
#22084=CARTESIAN_POINT('Origin',(0.,0.,0.));
#22085=CARTESIAN_POINT('',(-0.41,-5.02105187650415E-17,0.1));
#22086=CARTESIAN_POINT('Origin',(0.,0.,0.1));
#22087=CARTESIAN_POINT('',(-0.41,-5.02105187650415E-17,0.));
#22088=CARTESIAN_POINT('',(-0.41,-5.02105187650415E-17,0.));
#22089=CARTESIAN_POINT('Origin',(0.,0.,0.));
#22090=CARTESIAN_POINT('Origin',(0.,0.,0.));
#22091=CARTESIAN_POINT('',(-0.6,-7.34788079488412E-17,0.1));
#22092=CARTESIAN_POINT('Origin',(0.,0.,0.1));
#22093=CARTESIAN_POINT('',(-0.6,-7.34788079488412E-17,0.));
#22094=CARTESIAN_POINT('',(-0.6,-7.34788079488412E-17,0.));
#22095=CARTESIAN_POINT('Origin',(0.,0.,0.));
#22096=CARTESIAN_POINT('Origin',(0.,0.,0.1));
#22097=CARTESIAN_POINT('Origin',(0.,0.,0.));
#22116=UNCERTAINTY_MEASURE_WITH_UNIT(LENGTH_MEASURE(0.001),#22130,
'DISTANCE_ACCURACY_VALUE',
'Maximum model space distance between geometric entities at asserted c
onnectivities');
#22117=UNCERTAINTY_MEASURE_WITH_UNIT(LENGTH_MEASURE(0.001),#22130,
'DISTANCE_ACCURACY_VALUE',
'Maximum model space distance between geometric entities at asserted c
onnectivities');
#22128=(
GEOMETRIC_REPRESENTATION_CONTEXT(3)
GLOBAL_UNCERTAINTY_ASSIGNED_CONTEXT((#22116))
GLOBAL_UNIT_ASSIGNED_CONTEXT((#22130,#22132,#22133))
REPRESENTATION_CONTEXT('','3D')
);
#22129=(
GEOMETRIC_REPRESENTATION_CONTEXT(3)
GLOBAL_UNCERTAINTY_ASSIGNED_CONTEXT((#22117))
GLOBAL_UNIT_ASSIGNED_CONTEXT((#22130,#22132,#22133))
REPRESENTATION_CONTEXT('','3D')
);
#22130=(
LENGTH_UNIT()
NAMED_UNIT(*)
SI_UNIT(.CENTI.,.METRE.)
);
#22132=(
NAMED_UNIT(*)
PLANE_ANGLE_UNIT()
SI_UNIT($,.RADIAN.)
);
#22133=(
NAMED_UNIT(*)
SI_UNIT($,.STERADIAN.)
SOLID_ANGLE_UNIT()
);
#22144=SHAPE_DEFINITION_REPRESENTATION(#22163,#22182);
#22163=PRODUCT_DEFINITION_SHAPE('',$,#22194);
#22182=SHAPE_REPRESENTATION('',(#9483),#22128);
#22183=PRODUCT_DEFINITION_CONTEXT('part definition',#22218,'design');
#22194=PRODUCT_DEFINITION('Pivot thrust washer','Pivot thrust washer',#22205,
#22183);
#22205=PRODUCT_DEFINITION_FORMATION('',$,#22230);
#22218=APPLICATION_CONTEXT(
'Core Data for Automotive Mechanical Design Process');
#22219=PRODUCT_CONTEXT('part definition',#22218,'mechanical');
#22230=PRODUCT('Pivot thrust washer','Pivot thrust washer',$,(#22219));
#22238=PRESENTATION_STYLE_ASSIGNMENT((#22246));
#22246=SURFACE_STYLE_USAGE(.BOTH.,#22254);
#22254=SURFACE_SIDE_STYLE('',(#22262));
#22262=SURFACE_STYLE_FILL_AREA(#22270);
#22270=FILL_AREA_STYLE('Washer gray',(#22278));
#22278=FILL_AREA_STYLE_COLOUR('Washer gray',#22286);
#22286=COLOUR_RGB('Washer gray',0.725490196078431,0.752941176470588,0.792156862745098);
ENDSEC;
END-ISO-10303-21;
